ISO-10303-21;
HEADER;
/* Generated by software containing ST-Developer
 * from STEP Tools, Inc. (www.steptools.com) 
 */

FILE_DESCRIPTION(
/* description */ (''),
/* implementation_level */ '2;1');

FILE_NAME(
/* name */ '7-3.step',
/* time_stamp */ '2026-10-06T01:16:10-07:00',
/* author */ (''),
/* organization */ (''),
/* preprocessor_version */ 'ST-DEVELOPER v20.2',
/* originating_system */ 'Autodesk Translation Framework v15.15.0.0',
/* authorisation */ '');

FILE_SCHEMA (('AUTOMOTIVE_DESIGN { 1 0 10303 214 3 1 1 }'));
ENDSEC;

DATA;
#10=MECHANICAL_DESIGN_GEOMETRIC_PRESENTATION_REPRESENTATION('',(#311),#17113);
#189=B_SPLINE_CURVE_WITH_KNOTS('',3,(#11014,#11015,#11016,#11017,#11018,
#11019,#11020,#11021,#11022,#11023,#11024,#11025,#11026,#11027,#11028,#11029,
#11030,#11031),.UNSPECIFIED.,.F.,.F.,(4,2,2,2,2,2,2,2,4),(-0.576585828155656,
-0.528602590239897,-0.480619352324139,-0.432504952213955,-0.384390552103771,
-0.336276151993587,-0.288161751883402,-0.240178513967644,-0.192195276051885),
 .UNSPECIFIED.);
#190=B_SPLINE_CURVE_WITH_KNOTS('',3,(#11035,#11036,#11037,#11038,#11039,
#11040,#11041,#11042,#11043,#11044,#11045,#11046,#11047,#11048,#11049,#11050,
#11051,#11052),.UNSPECIFIED.,.F.,.F.,(4,2,2,2,2,2,2,2,4),(0.192195276051885,
0.240178513967643,0.288161751883402,0.336276151993586,0.38439055210377,
0.432504952213954,0.480619352324138,0.528602590239897,0.576585828155655),
 .UNSPECIFIED.);
#191=B_SPLINE_CURVE_WITH_KNOTS('',3,(#11054,#11055,#11056,#11057,#11058,
#11059,#11060,#11061,#11062,#11063,#11064,#11065,#11066,#11067,#11068,#11069,
#11070,#11071,#11072),.UNSPECIFIED.,.F.,.F.,(4,2,2,2,3,2,2,2,4),(0.576585828155655,
0.624569066071413,0.672552303987172,0.720666704097356,0.76878110420754,
0.816895504317724,0.865009904427908,0.912993142343667,0.960976380259425),
 .UNSPECIFIED.);
#192=B_SPLINE_CURVE_WITH_KNOTS('',3,(#11073,#11074,#11075,#11076,#11077,
#11078,#11079,#11080,#11081,#11082,#11083,#11084,#11085,#11086,#11087,#11088,
#11089,#11090,#11091),.UNSPECIFIED.,.F.,.F.,(4,2,2,2,3,2,2,2,4),(-0.192195276051885,
-0.144212038136127,-0.0962288002203689,-0.0481144001101845,0.,0.0481144001101841,
0.0962288002203682,0.144212038136126,0.192195276051885),.UNSPECIFIED.);
#193=B_SPLINE_CURVE_WITH_KNOTS('',3,(#11094,#11095,#11096,#11097,#11098,
#11099,#11100,#11101,#11102,#11103,#11104,#11105,#11106,#11107,#11108,#11109,
#11110,#11111,#11112),.UNSPECIFIED.,.F.,.F.,(4,2,2,2,3,2,2,2,4),(0.576585828155656,
0.624569066071414,0.672552303987172,0.720666704097356,0.76878110420754,
0.816895504317725,0.865009904427909,0.912993142343667,0.960976380259426),
 .UNSPECIFIED.);
#194=B_SPLINE_CURVE_WITH_KNOTS('',3,(#11113,#11114,#11115,#11116,#11117,
#11118,#11119,#11120,#11121,#11122,#11123,#11124,#11125,#11126,#11127,#11128,
#11129,#11130),.UNSPECIFIED.,.F.,.F.,(4,2,2,2,2,2,2,2,4),(0.960976380259426,
1.00895961817518,1.05694285609094,1.10505725620113,1.15317165631131,1.2012860564215,
1.24940045653168,1.29738369444744,1.3453669323632),.UNSPECIFIED.);
#195=B_SPLINE_CURVE_WITH_KNOTS('',3,(#11132,#11133,#11134,#11135,#11136,
#11137,#11138,#11139,#11140,#11141,#11142,#11143,#11144,#11145,#11146,#11147,
#11148,#11149,#11150,#11151,#11152,#11153,#11154,#11155,#11156,#11157,#11158,
#11159,#11160,#11161,#11162,#11163,#11164,#11165),.UNSPECIFIED.,.T.,.F.,
(4,2,2,2,2,2,2,2,2,2,2,2,2,2,2,2,4),(0.,0.0481144001101842,0.0962288002203683,
0.144212038136127,0.192195276051885,0.240178513967643,0.288161751883402,
0.336276151993586,0.38439055210377,0.432504952213954,0.480619352324138,
0.528602590239897,0.576585828155655,0.624569066071413,0.672552303987172,
0.720666704097356,0.76878110420754),.UNSPECIFIED.);
#271=SHAPE_REPRESENTATION_RELATIONSHIP('SRR','None',#17195,#287);
#287=ADVANCED_BREP_SHAPE_REPRESENTATION('',(#337),#17102);
#311=STYLED_ITEM('',(#17298),#337);
#337=MANIFOLD_SOLID_BREP('Body1',#6023);
#445=CYLINDRICAL_SURFACE('',#6682,2.5);
#446=CYLINDRICAL_SURFACE('',#6684,1.25);
#447=CYLINDRICAL_SURFACE('',#6686,1.25);
#448=CYLINDRICAL_SURFACE('',#6689,1.25);
#449=CYLINDRICAL_SURFACE('',#6691,1.25);
#586=FACE_BOUND('',#1675,.T.);
#587=FACE_BOUND('',#1676,.T.);
#869=CIRCLE('',#6681,2.5);
#870=CIRCLE('',#6683,2.5);
#871=CIRCLE('',#6685,1.25);
#872=CIRCLE('',#6687,1.25);
#873=CIRCLE('',#6690,1.25);
#874=CIRCLE('',#6692,1.25);
#1231=FACE_OUTER_BOUND('',#1673,.T.);
#1232=FACE_OUTER_BOUND('',#1674,.T.);
#1233=FACE_OUTER_BOUND('',#1677,.T.);
#1234=FACE_OUTER_BOUND('',#1678,.T.);
#1235=FACE_OUTER_BOUND('',#1679,.T.);
#1236=FACE_OUTER_BOUND('',#1680,.T.);
#1237=FACE_OUTER_BOUND('',#1681,.T.);
#1238=FACE_OUTER_BOUND('',#1682,.T.);
#1239=FACE_OUTER_BOUND('',#1683,.T.);
#1240=FACE_OUTER_BOUND('',#1684,.T.);
#1241=FACE_OUTER_BOUND('',#1685,.T.);
#1673=EDGE_LOOP('',(#4940));
#1674=EDGE_LOOP('',(#4941,#4942,#4943,#4944,#4945,#4946,#4947,#4948,#4949,
#4950,#4951,#4952));
#1675=EDGE_LOOP('',(#4953,#4954));
#1676=EDGE_LOOP('',(#4955));
#1677=EDGE_LOOP('',(#4956,#4957,#4958,#4959,#4960));
#1678=EDGE_LOOP('',(#4961,#4962,#4963,#4964,#4965));
#1679=EDGE_LOOP('',(#4966));
#1680=EDGE_LOOP('',(#4967,#4968,#4969,#4970,#4971));
#1681=EDGE_LOOP('',(#4972,#4973,#4974,#4975));
#1682=EDGE_LOOP('',(#4976));
#1683=EDGE_LOOP('',(#4977));
#1684=EDGE_LOOP('',(#4978));
#1685=EDGE_LOOP('',(#4979));
#2100=LINE('',#11012,#2461);
#2101=LINE('',#11033,#2462);
#2102=LINE('',#11053,#2463);
#2103=LINE('',#11169,#2464);
#2104=LINE('',#11172,#2465);
#2105=LINE('',#11177,#2466);
#2106=LINE('',#11182,#2467);
#2461=VECTOR('',#8168,2.5);
#2462=VECTOR('',#8169,2.5);
#2463=VECTOR('',#8170,2.5);
#2464=VECTOR('',#8175,1.25);
#2465=VECTOR('',#8178,1.25);
#2466=VECTOR('',#8185,1.25);
#2467=VECTOR('',#8192,1.25);
#2909=VERTEX_POINT('',#11006);
#2910=VERTEX_POINT('',#11009);
#2911=VERTEX_POINT('',#11011);
#2912=VERTEX_POINT('',#11013);
#2913=VERTEX_POINT('',#11032);
#2914=VERTEX_POINT('',#11034);
#2915=VERTEX_POINT('',#11092);
#2916=VERTEX_POINT('',#11093);
#2917=VERTEX_POINT('',#11131);
#2918=VERTEX_POINT('',#11167);
#2919=VERTEX_POINT('',#11171);
#2920=VERTEX_POINT('',#11176);
#2921=VERTEX_POINT('',#11180);
#3624=EDGE_CURVE('',#2909,#2909,#869,.T.);
#3625=EDGE_CURVE('',#2910,#2910,#870,.T.);
#3626=EDGE_CURVE('',#2910,#2911,#2100,.T.);
#3627=EDGE_CURVE('',#2912,#2911,#189,.T.);
#3628=EDGE_CURVE('',#2912,#2913,#2101,.T.);
#3629=EDGE_CURVE('',#2914,#2913,#190,.T.);
#3630=EDGE_CURVE('',#2914,#2909,#2102,.T.);
#3631=EDGE_CURVE('',#2913,#2914,#191,.T.);
#3632=EDGE_CURVE('',#2911,#2912,#192,.T.);
#3633=EDGE_CURVE('',#2915,#2916,#193,.T.);
#3634=EDGE_CURVE('',#2916,#2915,#194,.T.);
#3635=EDGE_CURVE('',#2917,#2917,#195,.T.);
#3636=EDGE_CURVE('',#2918,#2918,#871,.T.);
#3637=EDGE_CURVE('',#2918,#2916,#2103,.T.);
#3638=EDGE_CURVE('',#2911,#2919,#2104,.T.);
#3639=EDGE_CURVE('',#2919,#2919,#872,.T.);
#3640=EDGE_CURVE('',#2913,#2920,#2105,.T.);
#3641=EDGE_CURVE('',#2920,#2920,#873,.T.);
#3642=EDGE_CURVE('',#2921,#2921,#874,.T.);
#3643=EDGE_CURVE('',#2921,#2917,#2106,.T.);
#4940=ORIENTED_EDGE('',*,*,#3624,.F.);
#4941=ORIENTED_EDGE('',*,*,#3625,.F.);
#4942=ORIENTED_EDGE('',*,*,#3626,.T.);
#4943=ORIENTED_EDGE('',*,*,#3627,.F.);
#4944=ORIENTED_EDGE('',*,*,#3628,.T.);
#4945=ORIENTED_EDGE('',*,*,#3629,.F.);
#4946=ORIENTED_EDGE('',*,*,#3630,.T.);
#4947=ORIENTED_EDGE('',*,*,#3624,.T.);
#4948=ORIENTED_EDGE('',*,*,#3630,.F.);
#4949=ORIENTED_EDGE('',*,*,#3631,.F.);
#4950=ORIENTED_EDGE('',*,*,#3628,.F.);
#4951=ORIENTED_EDGE('',*,*,#3632,.F.);
#4952=ORIENTED_EDGE('',*,*,#3626,.F.);
#4953=ORIENTED_EDGE('',*,*,#3633,.F.);
#4954=ORIENTED_EDGE('',*,*,#3634,.F.);
#4955=ORIENTED_EDGE('',*,*,#3635,.F.);
#4956=ORIENTED_EDGE('',*,*,#3636,.F.);
#4957=ORIENTED_EDGE('',*,*,#3637,.T.);
#4958=ORIENTED_EDGE('',*,*,#3634,.T.);
#4959=ORIENTED_EDGE('',*,*,#3633,.T.);
#4960=ORIENTED_EDGE('',*,*,#3637,.F.);
#4961=ORIENTED_EDGE('',*,*,#3627,.T.);
#4962=ORIENTED_EDGE('',*,*,#3638,.T.);
#4963=ORIENTED_EDGE('',*,*,#3639,.T.);
#4964=ORIENTED_EDGE('',*,*,#3638,.F.);
#4965=ORIENTED_EDGE('',*,*,#3632,.T.);
#4966=ORIENTED_EDGE('',*,*,#3625,.T.);
#4967=ORIENTED_EDGE('',*,*,#3629,.T.);
#4968=ORIENTED_EDGE('',*,*,#3640,.T.);
#4969=ORIENTED_EDGE('',*,*,#3641,.T.);
#4970=ORIENTED_EDGE('',*,*,#3640,.F.);
#4971=ORIENTED_EDGE('',*,*,#3631,.T.);
#4972=ORIENTED_EDGE('',*,*,#3642,.F.);
#4973=ORIENTED_EDGE('',*,*,#3643,.T.);
#4974=ORIENTED_EDGE('',*,*,#3635,.T.);
#4975=ORIENTED_EDGE('',*,*,#3643,.F.);
#4976=ORIENTED_EDGE('',*,*,#3636,.T.);
#4977=ORIENTED_EDGE('',*,*,#3642,.T.);
#4978=ORIENTED_EDGE('',*,*,#3639,.F.);
#4979=ORIENTED_EDGE('',*,*,#3641,.F.);
#5592=PLANE('',#6680);
#5593=PLANE('',#6688);
#5594=PLANE('',#6693);
#5595=PLANE('',#6694);
#5596=PLANE('',#6695);
#5597=PLANE('',#6696);
#5879=ADVANCED_FACE('',(#1231),#5592,.F.);
#5880=ADVANCED_FACE('',(#1232,#586,#587),#445,.T.);
#5881=ADVANCED_FACE('',(#1233),#446,.T.);
#5882=ADVANCED_FACE('',(#1234),#447,.T.);
#5883=ADVANCED_FACE('',(#1235),#5593,.T.);
#5884=ADVANCED_FACE('',(#1236),#448,.T.);
#5885=ADVANCED_FACE('',(#1237),#449,.T.);
#5886=ADVANCED_FACE('',(#1238),#5594,.T.);
#5887=ADVANCED_FACE('',(#1239),#5595,.T.);
#5888=ADVANCED_FACE('',(#1240),#5596,.F.);
#5889=ADVANCED_FACE('',(#1241),#5597,.F.);
#6023=CLOSED_SHELL('',(#5879,#5880,#5881,#5882,#5883,#5884,#5885,#5886,
#5887,#5888,#5889));
#6679=AXIS2_PLACEMENT_3D('',#11004,#8158,#8159);
#6680=AXIS2_PLACEMENT_3D('',#11005,#8160,#8161);
#6681=AXIS2_PLACEMENT_3D('',#11007,#8162,#8163);
#6682=AXIS2_PLACEMENT_3D('',#11008,#8164,#8165);
#6683=AXIS2_PLACEMENT_3D('',#11010,#8166,#8167);
#6684=AXIS2_PLACEMENT_3D('',#11166,#8171,#8172);
#6685=AXIS2_PLACEMENT_3D('',#11168,#8173,#8174);
#6686=AXIS2_PLACEMENT_3D('',#11170,#8176,#8177);
#6687=AXIS2_PLACEMENT_3D('',#11173,#8179,#8180);
#6688=AXIS2_PLACEMENT_3D('',#11174,#8181,#8182);
#6689=AXIS2_PLACEMENT_3D('',#11175,#8183,#8184);
#6690=AXIS2_PLACEMENT_3D('',#11178,#8186,#8187);
#6691=AXIS2_PLACEMENT_3D('',#11179,#8188,#8189);
#6692=AXIS2_PLACEMENT_3D('',#11181,#8190,#8191);
#6693=AXIS2_PLACEMENT_3D('',#11183,#8193,#8194);
#6694=AXIS2_PLACEMENT_3D('',#11184,#8195,#8196);
#6695=AXIS2_PLACEMENT_3D('',#11185,#8197,#8198);
#6696=AXIS2_PLACEMENT_3D('',#11186,#8199,#8200);
#8158=DIRECTION('axis',(0.,0.,1.));
#8159=DIRECTION('refdir',(1.,0.,0.));
#8160=DIRECTION('center_axis',(0.,1.,0.));
#8161=DIRECTION('ref_axis',(1.,0.,0.));
#8162=DIRECTION('center_axis',(0.,1.,0.));
#8163=DIRECTION('ref_axis',(1.,0.,0.));
#8164=DIRECTION('center_axis',(0.,1.,0.));
#8165=DIRECTION('ref_axis',(1.,0.,0.));
#8166=DIRECTION('center_axis',(0.,1.,0.));
#8167=DIRECTION('ref_axis',(1.,0.,0.));
#8168=DIRECTION('',(0.,-1.,0.));
#8169=DIRECTION('',(0.,-1.,0.));
#8170=DIRECTION('',(0.,-1.,0.));
#8171=DIRECTION('center_axis',(1.,0.,0.));
#8172=DIRECTION('ref_axis',(0.,-1.,0.));
#8173=DIRECTION('center_axis',(1.,0.,0.));
#8174=DIRECTION('ref_axis',(0.,-1.,0.));
#8175=DIRECTION('',(-1.,0.,0.));
#8176=DIRECTION('center_axis',(1.,0.,0.));
#8177=DIRECTION('ref_axis',(0.,-1.,0.));
#8178=DIRECTION('',(-1.,0.,0.));
#8179=DIRECTION('center_axis',(1.,0.,0.));
#8180=DIRECTION('ref_axis',(0.,-1.,0.));
#8181=DIRECTION('center_axis',(0.,1.,0.));
#8182=DIRECTION('ref_axis',(1.,0.,0.));
#8183=DIRECTION('center_axis',(1.,0.,0.));
#8184=DIRECTION('ref_axis',(0.,-1.,0.));
#8185=DIRECTION('',(-1.,0.,0.));
#8186=DIRECTION('center_axis',(1.,0.,0.));
#8187=DIRECTION('ref_axis',(0.,1.,0.));
#8188=DIRECTION('center_axis',(1.,0.,0.));
#8189=DIRECTION('ref_axis',(0.,-1.,0.));
#8190=DIRECTION('center_axis',(1.,0.,0.));
#8191=DIRECTION('ref_axis',(0.,1.,0.));
#8192=DIRECTION('',(-1.,0.,0.));
#8193=DIRECTION('center_axis',(1.,0.,0.));
#8194=DIRECTION('ref_axis',(0.,-1.,0.));
#8195=DIRECTION('center_axis',(1.,0.,0.));
#8196=DIRECTION('ref_axis',(0.,-1.,0.));
#8197=DIRECTION('center_axis',(1.,0.,0.));
#8198=DIRECTION('ref_axis',(0.,-1.,0.));
#8199=DIRECTION('center_axis',(1.,0.,0.));
#8200=DIRECTION('ref_axis',(0.,-1.,0.));
#11004=CARTESIAN_POINT('',(0.,0.,0.));
#11005=CARTESIAN_POINT('Origin',(0.,-22.5,0.));
#11006=CARTESIAN_POINT('',(-2.5,-22.5,0.));
#11007=CARTESIAN_POINT('Origin',(0.,-22.5,0.));
#11008=CARTESIAN_POINT('Origin',(0.,-22.5,0.));
#11009=CARTESIAN_POINT('',(-2.5,22.5,3.06161699786838E-16));
#11010=CARTESIAN_POINT('Origin',(0.,22.5,0.));
#11011=CARTESIAN_POINT('',(-2.5,19.75,6.63446760945788E-17));
#11012=CARTESIAN_POINT('',(-2.5,-22.5,3.06161699786838E-16));
#11013=CARTESIAN_POINT('',(-2.5,17.25,0.));
#11014=CARTESIAN_POINT('Ctrl Pts',(-2.5,17.25,3.12250225675825E-16));
#11015=CARTESIAN_POINT('Ctrl Pts',(-2.5,17.25,0.159944126385861));
#11016=CARTESIAN_POINT('Ctrl Pts',(-2.48323996043832,17.2825451176636,0.328681344361068));
#11017=CARTESIAN_POINT('Ctrl Pts',(-2.42283105129935,17.4110436500943,0.635925947642967));
#11018=CARTESIAN_POINT('Ctrl Pts',(-2.37983326258812,17.5068538842915,0.774620837257827));
#11019=CARTESIAN_POINT('Ctrl Pts',(-2.29712558443605,17.7256778321974,0.993444785163792));
#11020=CARTESIAN_POINT('Ctrl Pts',(-2.25149501557585,17.8642720506152,1.08903588717028));
#11021=CARTESIAN_POINT('Ctrl Pts',(-2.18478179494117,18.1710767484209,1.21735698059595));
#11022=CARTESIAN_POINT('Ctrl Pts',(-2.1650635094611,18.3396186662994,1.25));
#11023=CARTESIAN_POINT('Ctrl Pts',(-2.1650635094611,18.6603813337006,1.25));
#11024=CARTESIAN_POINT('Ctrl Pts',(-2.18478179494117,18.8289232515791,1.21735698059595));
#11025=CARTESIAN_POINT('Ctrl Pts',(-2.25149501557585,19.1357279493848,1.08903588717028));
#11026=CARTESIAN_POINT('Ctrl Pts',(-2.29712558443604,19.2743221678026,0.993444785163795));
#11027=CARTESIAN_POINT('Ctrl Pts',(-2.37983326258812,19.4931461157085,0.77462083725783));
#11028=CARTESIAN_POINT('Ctrl Pts',(-2.42283105129935,19.5889563499057,0.63592594764297));
#11029=CARTESIAN_POINT('Ctrl Pts',(-2.48323996043832,19.7174548823364,0.328681344361071));
#11030=CARTESIAN_POINT('Ctrl Pts',(-2.5,19.75,0.159944126385861));
#11031=CARTESIAN_POINT('Ctrl Pts',(-2.5,19.75,-3.46944695195361E-16));
#11032=CARTESIAN_POINT('',(-2.5,-17.75,1.35733615133651E-16));
#11033=CARTESIAN_POINT('',(-2.5,-22.5,3.06161699786838E-16));
#11034=CARTESIAN_POINT('',(-2.5,-20.25,0.));
#11035=CARTESIAN_POINT('Ctrl Pts',(-2.5,-20.25,1.73472347597681E-16));
#11036=CARTESIAN_POINT('Ctrl Pts',(-2.5,-20.25,0.159944126385861));
#11037=CARTESIAN_POINT('Ctrl Pts',(-2.48323996043832,-20.2174548823364,
0.32868134436107));
#11038=CARTESIAN_POINT('Ctrl Pts',(-2.42283105129935,-20.0889563499057,
0.635925947642969));
#11039=CARTESIAN_POINT('Ctrl Pts',(-2.37983326258812,-19.9931461157085,
0.774620837257828));
#11040=CARTESIAN_POINT('Ctrl Pts',(-2.29712558443605,-19.7743221678026,
0.993444785163793));
#11041=CARTESIAN_POINT('Ctrl Pts',(-2.25149501557585,-19.6357279493848,
1.08903588717028));
#11042=CARTESIAN_POINT('Ctrl Pts',(-2.18478179494117,-19.3289232515791,
1.21735698059595));
#11043=CARTESIAN_POINT('Ctrl Pts',(-2.1650635094611,-19.1603813337006,1.25));
#11044=CARTESIAN_POINT('Ctrl Pts',(-2.1650635094611,-18.8396186662994,1.25));
#11045=CARTESIAN_POINT('Ctrl Pts',(-2.18478179494117,-18.6710767484209,
1.21735698059595));
#11046=CARTESIAN_POINT('Ctrl Pts',(-2.25149501557585,-18.3642720506152,
1.08903588717028));
#11047=CARTESIAN_POINT('Ctrl Pts',(-2.29712558443605,-18.2256778321974,
0.993444785163793));
#11048=CARTESIAN_POINT('Ctrl Pts',(-2.37983326258812,-18.0068538842915,
0.774620837257828));
#11049=CARTESIAN_POINT('Ctrl Pts',(-2.42283105129935,-17.9110436500943,
0.635925947642967));
#11050=CARTESIAN_POINT('Ctrl Pts',(-2.48323996043832,-17.7825451176636,
0.328681344361068));
#11051=CARTESIAN_POINT('Ctrl Pts',(-2.5,-17.75,0.159944126385861));
#11052=CARTESIAN_POINT('Ctrl Pts',(-2.5,-17.75,2.77555756156289E-16));
#11053=CARTESIAN_POINT('',(-2.5,-22.5,3.06161699786838E-16));
#11054=CARTESIAN_POINT('Ctrl Pts',(-2.5,-17.75,-1.38777878078145E-16));
#11055=CARTESIAN_POINT('Ctrl Pts',(-2.5,-17.75,-0.159944126385861));
#11056=CARTESIAN_POINT('Ctrl Pts',(-2.48323996043832,-17.7825451176636,
-0.328681344361068));
#11057=CARTESIAN_POINT('Ctrl Pts',(-2.42283105129935,-17.9110436500943,
-0.635925947642967));
#11058=CARTESIAN_POINT('Ctrl Pts',(-2.37983326258812,-18.0068538842915,
-0.774620837257828));
#11059=CARTESIAN_POINT('Ctrl Pts',(-2.29712558443605,-18.2256778321974,
-0.993444785163793));
#11060=CARTESIAN_POINT('Ctrl Pts',(-2.25149501557585,-18.3642720506152,
-1.08903588717028));
#11061=CARTESIAN_POINT('Ctrl Pts',(-2.18478179494117,-18.6710767484209,
-1.21735698059595));
#11062=CARTESIAN_POINT('Ctrl Pts',(-2.1650635094611,-18.8396186662994,-1.25));
#11063=CARTESIAN_POINT('Ctrl Pts',(-2.1650635094611,-19.,-1.25));
#11064=CARTESIAN_POINT('Ctrl Pts',(-2.1650635094611,-19.1603813337006,-1.25));
#11065=CARTESIAN_POINT('Ctrl Pts',(-2.18478179494117,-19.3289232515791,
-1.21735698059595));
#11066=CARTESIAN_POINT('Ctrl Pts',(-2.25149501557585,-19.6357279493848,
-1.08903588717028));
#11067=CARTESIAN_POINT('Ctrl Pts',(-2.29712558443605,-19.7743221678026,
-0.993444785163793));
#11068=CARTESIAN_POINT('Ctrl Pts',(-2.37983326258812,-19.9931461157085,
-0.774620837257828));
#11069=CARTESIAN_POINT('Ctrl Pts',(-2.42283105129935,-20.0889563499057,
-0.635925947642969));
#11070=CARTESIAN_POINT('Ctrl Pts',(-2.48323996043832,-20.2174548823364,
-0.32868134436107));
#11071=CARTESIAN_POINT('Ctrl Pts',(-2.5,-20.25,-0.159944126385861));
#11072=CARTESIAN_POINT('Ctrl Pts',(-2.5,-20.25,-1.38777878078145E-16));
#11073=CARTESIAN_POINT('Ctrl Pts',(-2.5,19.75,-1.73472347597681E-16));
#11074=CARTESIAN_POINT('Ctrl Pts',(-2.5,19.75,-0.159944126385861));
#11075=CARTESIAN_POINT('Ctrl Pts',(-2.48323996043832,19.7174548823364,-0.328681344361069));
#11076=CARTESIAN_POINT('Ctrl Pts',(-2.42283105129935,19.5889563499057,-0.635925947642968));
#11077=CARTESIAN_POINT('Ctrl Pts',(-2.37983326258812,19.4931461157085,-0.77462083725783));
#11078=CARTESIAN_POINT('Ctrl Pts',(-2.29712558443604,19.2743221678026,-0.993444785163795));
#11079=CARTESIAN_POINT('Ctrl Pts',(-2.25149501557585,19.1357279493848,-1.08903588717028));
#11080=CARTESIAN_POINT('Ctrl Pts',(-2.18478179494117,18.8289232515791,-1.21735698059595));
#11081=CARTESIAN_POINT('Ctrl Pts',(-2.1650635094611,18.6603813337006,-1.25));
#11082=CARTESIAN_POINT('Ctrl Pts',(-2.1650635094611,18.5,-1.25));
#11083=CARTESIAN_POINT('Ctrl Pts',(-2.1650635094611,18.3396186662994,-1.25));
#11084=CARTESIAN_POINT('Ctrl Pts',(-2.18478179494117,18.1710767484209,-1.21735698059595));
#11085=CARTESIAN_POINT('Ctrl Pts',(-2.25149501557585,17.8642720506152,-1.08903588717028));
#11086=CARTESIAN_POINT('Ctrl Pts',(-2.29712558443605,17.7256778321974,-0.993444785163791));
#11087=CARTESIAN_POINT('Ctrl Pts',(-2.37983326258812,17.5068538842915,-0.774620837257827));
#11088=CARTESIAN_POINT('Ctrl Pts',(-2.42283105129935,17.4110436500943,-0.635925947642967));
#11089=CARTESIAN_POINT('Ctrl Pts',(-2.48323996043832,17.2825451176636,-0.328681344361068));
#11090=CARTESIAN_POINT('Ctrl Pts',(-2.5,17.25,-0.15994412638586));
#11091=CARTESIAN_POINT('Ctrl Pts',(-2.5,17.25,2.42861286636753E-16));
#11092=CARTESIAN_POINT('',(2.5,17.25,0.));
#11093=CARTESIAN_POINT('',(2.5,19.75,4.92874059181143E-16));
#11094=CARTESIAN_POINT('Ctrl Pts',(2.5,17.25,-1.38777878078145E-16));
#11095=CARTESIAN_POINT('Ctrl Pts',(2.5,17.25,-0.159944126385861));
#11096=CARTESIAN_POINT('Ctrl Pts',(2.48323996043832,17.2825451176636,-0.328681344361068));
#11097=CARTESIAN_POINT('Ctrl Pts',(2.42283105129935,17.4110436500943,-0.635925947642967));
#11098=CARTESIAN_POINT('Ctrl Pts',(2.37983326258812,17.5068538842915,-0.774620837257827));
#11099=CARTESIAN_POINT('Ctrl Pts',(2.29712558443605,17.7256778321974,-0.993444785163792));
#11100=CARTESIAN_POINT('Ctrl Pts',(2.25149501557585,17.8642720506152,-1.08903588717028));
#11101=CARTESIAN_POINT('Ctrl Pts',(2.18478179494117,18.1710767484209,-1.21735698059595));
#11102=CARTESIAN_POINT('Ctrl Pts',(2.1650635094611,18.3396186662994,-1.25));
#11103=CARTESIAN_POINT('Ctrl Pts',(2.1650635094611,18.5,-1.25));
#11104=CARTESIAN_POINT('Ctrl Pts',(2.1650635094611,18.6603813337006,-1.25));
#11105=CARTESIAN_POINT('Ctrl Pts',(2.18478179494117,18.8289232515791,-1.21735698059595));
#11106=CARTESIAN_POINT('Ctrl Pts',(2.25149501557585,19.1357279493848,-1.08903588717028));
#11107=CARTESIAN_POINT('Ctrl Pts',(2.29712558443604,19.2743221678026,-0.993444785163795));
#11108=CARTESIAN_POINT('Ctrl Pts',(2.37983326258812,19.4931461157085,-0.77462083725783));
#11109=CARTESIAN_POINT('Ctrl Pts',(2.42283105129935,19.5889563499057,-0.635925947642969));
#11110=CARTESIAN_POINT('Ctrl Pts',(2.48323996043832,19.7174548823364,-0.32868134436107));
#11111=CARTESIAN_POINT('Ctrl Pts',(2.5,19.75,-0.159944126385861));
#11112=CARTESIAN_POINT('Ctrl Pts',(2.5,19.75,1.04083408558608E-16));
#11113=CARTESIAN_POINT('Ctrl Pts',(2.5,19.75,1.73472347597681E-16));
#11114=CARTESIAN_POINT('Ctrl Pts',(2.5,19.75,0.159944126385861));
#11115=CARTESIAN_POINT('Ctrl Pts',(2.48323996043832,19.7174548823364,0.328681344361071));
#11116=CARTESIAN_POINT('Ctrl Pts',(2.42283105129935,19.5889563499057,0.63592594764297));
#11117=CARTESIAN_POINT('Ctrl Pts',(2.37983326258812,19.4931461157085,0.77462083725783));
#11118=CARTESIAN_POINT('Ctrl Pts',(2.29712558443604,19.2743221678026,0.993444785163795));
#11119=CARTESIAN_POINT('Ctrl Pts',(2.25149501557585,19.1357279493848,1.08903588717028));
#11120=CARTESIAN_POINT('Ctrl Pts',(2.18478179494117,18.8289232515791,1.21735698059595));
#11121=CARTESIAN_POINT('Ctrl Pts',(2.1650635094611,18.6603813337006,1.25));
#11122=CARTESIAN_POINT('Ctrl Pts',(2.1650635094611,18.3396186662994,1.25));
#11123=CARTESIAN_POINT('Ctrl Pts',(2.18478179494117,18.1710767484209,1.21735698059595));
#11124=CARTESIAN_POINT('Ctrl Pts',(2.25149501557585,17.8642720506152,1.08903588717028));
#11125=CARTESIAN_POINT('Ctrl Pts',(2.29712558443605,17.7256778321974,0.993444785163791));
#11126=CARTESIAN_POINT('Ctrl Pts',(2.37983326258812,17.5068538842915,0.774620837257827));
#11127=CARTESIAN_POINT('Ctrl Pts',(2.42283105129935,17.4110436500943,0.635925947642967));
#11128=CARTESIAN_POINT('Ctrl Pts',(2.48323996043832,17.2825451176636,0.328681344361068));
#11129=CARTESIAN_POINT('Ctrl Pts',(2.5,17.25,0.159944126385861));
#11130=CARTESIAN_POINT('Ctrl Pts',(2.5,17.25,1.04083408558608E-16));
#11131=CARTESIAN_POINT('',(2.5,-17.75,0.));
#11132=CARTESIAN_POINT('Ctrl Pts',(2.1650635094611,-19.,-1.25));
#11133=CARTESIAN_POINT('Ctrl Pts',(2.1650635094611,-18.8396186662994,-1.25));
#11134=CARTESIAN_POINT('Ctrl Pts',(2.18478179494117,-18.6710767484209,-1.21735698059595));
#11135=CARTESIAN_POINT('Ctrl Pts',(2.25149501557585,-18.3642720506152,-1.08903588717028));
#11136=CARTESIAN_POINT('Ctrl Pts',(2.29712558443605,-18.2256778321974,-0.993444785163793));
#11137=CARTESIAN_POINT('Ctrl Pts',(2.37983326258812,-18.0068538842915,-0.774620837257828));
#11138=CARTESIAN_POINT('Ctrl Pts',(2.42283105129935,-17.9110436500943,-0.63592594764297));
#11139=CARTESIAN_POINT('Ctrl Pts',(2.48323996043832,-17.7825451176636,-0.328681344361071));
#11140=CARTESIAN_POINT('Ctrl Pts',(2.5,-17.75,-0.159944126385861));
#11141=CARTESIAN_POINT('Ctrl Pts',(2.5,-17.75,0.159944126385861));
#11142=CARTESIAN_POINT('Ctrl Pts',(2.48323996043832,-17.7825451176636,0.328681344361068));
#11143=CARTESIAN_POINT('Ctrl Pts',(2.42283105129935,-17.9110436500943,0.635925947642967));
#11144=CARTESIAN_POINT('Ctrl Pts',(2.37983326258812,-18.0068538842915,0.774620837257829));
#11145=CARTESIAN_POINT('Ctrl Pts',(2.29712558443605,-18.2256778321974,0.993444785163793));
#11146=CARTESIAN_POINT('Ctrl Pts',(2.25149501557585,-18.3642720506152,1.08903588717028));
#11147=CARTESIAN_POINT('Ctrl Pts',(2.18478179494117,-18.6710767484209,1.21735698059595));
#11148=CARTESIAN_POINT('Ctrl Pts',(2.1650635094611,-18.8396186662994,1.25));
#11149=CARTESIAN_POINT('Ctrl Pts',(2.1650635094611,-19.1603813337006,1.25));
#11150=CARTESIAN_POINT('Ctrl Pts',(2.18478179494117,-19.3289232515791,1.21735698059595));
#11151=CARTESIAN_POINT('Ctrl Pts',(2.25149501557585,-19.6357279493848,1.08903588717028));
#11152=CARTESIAN_POINT('Ctrl Pts',(2.29712558443605,-19.7743221678026,0.993444785163793));
#11153=CARTESIAN_POINT('Ctrl Pts',(2.37983326258812,-19.9931461157085,0.774620837257828));
#11154=CARTESIAN_POINT('Ctrl Pts',(2.42283105129935,-20.0889563499057,0.635925947642968));
#11155=CARTESIAN_POINT('Ctrl Pts',(2.48323996043832,-20.2174548823364,0.328681344361069));
#11156=CARTESIAN_POINT('Ctrl Pts',(2.5,-20.25,0.159944126385861));
#11157=CARTESIAN_POINT('Ctrl Pts',(2.5,-20.25,-0.159944126385861));
#11158=CARTESIAN_POINT('Ctrl Pts',(2.48323996043832,-20.2174548823364,-0.32868134436107));
#11159=CARTESIAN_POINT('Ctrl Pts',(2.42283105129935,-20.0889563499057,-0.635925947642969));
#11160=CARTESIAN_POINT('Ctrl Pts',(2.37983326258812,-19.9931461157085,-0.774620837257828));
#11161=CARTESIAN_POINT('Ctrl Pts',(2.29712558443605,-19.7743221678026,-0.993444785163793));
#11162=CARTESIAN_POINT('Ctrl Pts',(2.25149501557585,-19.6357279493848,-1.08903588717028));
#11163=CARTESIAN_POINT('Ctrl Pts',(2.18478179494117,-19.3289232515791,-1.21735698059595));
#11164=CARTESIAN_POINT('Ctrl Pts',(2.1650635094611,-19.1603813337006,-1.25));
#11165=CARTESIAN_POINT('Ctrl Pts',(2.1650635094611,-19.,-1.25));
#11166=CARTESIAN_POINT('Origin',(-6.,18.5,0.));
#11167=CARTESIAN_POINT('',(6.,19.75,1.53080849893419E-16));
#11168=CARTESIAN_POINT('Origin',(6.,18.5,0.));
#11169=CARTESIAN_POINT('',(-6.,19.75,1.53080849893419E-16));
#11170=CARTESIAN_POINT('Origin',(-6.,18.5,0.));
#11171=CARTESIAN_POINT('',(-6.,19.75,0.));
#11172=CARTESIAN_POINT('',(-6.,19.75,1.53080849893419E-16));
#11173=CARTESIAN_POINT('Origin',(-6.,18.5,0.));
#11174=CARTESIAN_POINT('Origin',(0.,22.5,0.));
#11175=CARTESIAN_POINT('Origin',(-6.,-19.,0.));
#11176=CARTESIAN_POINT('',(-6.,-17.75,1.53080849893419E-16));
#11177=CARTESIAN_POINT('',(-6.,-17.75,1.53080849893419E-16));
#11178=CARTESIAN_POINT('Origin',(-6.,-19.,0.));
#11179=CARTESIAN_POINT('Origin',(-6.,-19.,0.));
#11180=CARTESIAN_POINT('',(6.,-17.75,0.));
#11181=CARTESIAN_POINT('Origin',(6.,-19.,0.));
#11182=CARTESIAN_POINT('',(-6.,-17.75,1.53080849893419E-16));
#11183=CARTESIAN_POINT('Origin',(6.,0.,0.));
#11184=CARTESIAN_POINT('Origin',(6.,0.,0.));
#11185=CARTESIAN_POINT('Origin',(-6.,0.,0.));
#11186=CARTESIAN_POINT('Origin',(-6.,0.,0.));
#17079=UNCERTAINTY_MEASURE_WITH_UNIT(LENGTH_MEASURE(0.01),#17114,
'DISTANCE_ACCURACY_VALUE',
'Maximum model space distance between geometric entities at asserted c
onnectivities');
#17090=UNCERTAINTY_MEASURE_WITH_UNIT(LENGTH_MEASURE(0.01),#17114,
'DISTANCE_ACCURACY_VALUE',
'Maximum model space distance between geometric entities at asserted c
onnectivities');
#17102=(
GEOMETRIC_REPRESENTATION_CONTEXT(3)
GLOBAL_UNCERTAINTY_ASSIGNED_CONTEXT((#17079))
GLOBAL_UNIT_ASSIGNED_CONTEXT((#17114,#17116,#17117))
REPRESENTATION_CONTEXT('','3D')
);
#17113=(
GEOMETRIC_REPRESENTATION_CONTEXT(3)
GLOBAL_UNCERTAINTY_ASSIGNED_CONTEXT((#17090))
GLOBAL_UNIT_ASSIGNED_CONTEXT((#17114,#17116,#17117))
REPRESENTATION_CONTEXT('','3D')
);
#17114=(
LENGTH_UNIT()
NAMED_UNIT(*)
SI_UNIT(.MILLI.,.METRE.)
);
#17116=(
NAMED_UNIT(*)
PLANE_ANGLE_UNIT()
SI_UNIT($,.RADIAN.)
);
#17117=(
NAMED_UNIT(*)
SI_UNIT($,.STERADIAN.)
SOLID_ANGLE_UNIT()
);
#17129=SHAPE_DEFINITION_REPRESENTATION(#17155,#17195);
#17155=PRODUCT_DEFINITION_SHAPE('',$,#17218);
#17195=SHAPE_REPRESENTATION('',(#6679),#17102);
#17206=PRODUCT_DEFINITION_CONTEXT('part definition',#17274,'design');
#17218=PRODUCT_DEFINITION('7-3','7-3',#17240,#17206);
#17240=PRODUCT_DEFINITION_FORMATION('',$,#17287);
#17274=APPLICATION_CONTEXT(
'Core Data for Automotive Mechanical Design Process');
#17275=PRODUCT_CONTEXT('part definition',#17274,'mechanical');
#17287=PRODUCT('7-3','7-3','NOT SPECIFIED',(#17275));
#17298=PRESENTATION_STYLE_ASSIGNMENT((#17299));
#17299=SURFACE_STYLE_USAGE(.BOTH.,#17300);
#17300=SURFACE_SIDE_STYLE('',(#17301));
#17301=SURFACE_STYLE_FILL_AREA(#17302);
#17302=FILL_AREA_STYLE('Steel - Satin',(#17303));
#17303=FILL_AREA_STYLE_COLOUR('Steel - Satin',#17304);
#17304=COLOUR_RGB('Steel - Satin', 0.09019608, 0.27058824, 0.51372549);
ENDSEC;
END-ISO-10303-21;
